ISO-10303-21;
HEADER;
FILE_DESCRIPTION (('STEP AP214'),
    '1' );
FILE_NAME ('Precision Steel Bearing Balls.step',
    '2026-10-09T12:49:55',
    ( '' ),
    ( '' ),
    'SwSTEP 2.0',
    'SolidWorks 2026',
    '' );
FILE_SCHEMA (( 'AUTOMOTIVE_DESIGN' ));
ENDSEC;

DATA;
#81=CARTESIAN_POINT ( 'NONE',  ( 11.00000000000000000, 0.000000000000000000, 259.9000000000000341 ) ) ;
#165=SHAPE_REPRESENTATION_RELATIONSHIP ( 'NONE' , 'NONE' ,  #182, #11264 ) ;
#182=SHAPE_REPRESENTATION ( 'Precision Steel Bearing Balls', ( #805 ), #1451 ) ;
#240=CARTESIAN_POINT ( 'NONE',  ( 11.00000000000000000, 0.000000000000000000, 250.0000000000000000 ) ) ;
#292=PRODUCT_DEFINITION_CONTEXT ( 'detailed design', #12301, 'design' ) ;
#346=ADVANCED_FACE ( 'NONE', ( #6298 ), #7414, .T. ) ;
#370=EDGE_CURVE ( 'NONE', #690, #1431, #11004, .T. ) ;
#690=VERTEX_POINT ( 'NONE', #81 ) ;
#805=AXIS2_PLACEMENT_3D ( 'NONE', #6711, #10765, #10635 ) ;
#867=( LENGTH_UNIT ( ) NAMED_UNIT ( * ) SI_UNIT ( .MILLI., .METRE. ) );
#1431=VERTEX_POINT ( 'NONE', #13015 ) ;
#1451=( GEOMETRIC_REPRESENTATION_CONTEXT ( 3 ) GLOBAL_UNCERTAINTY_ASSIGNED_CONTEXT ( ( #7357 ) ) GLOBAL_UNIT_ASSIGNED_CONTEXT ( ( #9033, #8833, #10287 ) ) REPRESENTATION_CONTEXT ( 'NONE', 'WORKASPACE' ) );
#1793=PRODUCT_DEFINITION_SHAPE ( 'NONE', 'NONE',  #12069 ) ;
#1839=ORIENTED_EDGE ( 'NONE', *, *, #370, .T. ) ;
#1930=DIRECTION ( 'NONE',  ( 1.000000000000000000, 0.000000000000000000, 0.000000000000000000 ) ) ;
#2271=EDGE_LOOP ( 'NONE', ( #3914, #9287 ) ) ;
#2652=MECHANICAL_DESIGN_GEOMETRIC_PRESENTATION_REPRESENTATION('',(#12459),#9051);
#2781=SURFACE_SIDE_STYLE ('',( #9126 ) ) ;
#2848=SPHERICAL_SURFACE ( 'NONE', #11070, 9.900000000000000355 ) ;
#3116=AXIS2_PLACEMENT_3D ( 'NONE', #7356, #11489, #5613 ) ;
#3557=DIRECTION ( 'NONE',  ( 1.224646799147353207E-16, -1.000000000000000000, 0.000000000000000000 ) ) ;
#3758=AXIS2_PLACEMENT_3D ( 'NONE', #7873, #10874, #12938 ) ;
#3805=PRODUCT ( 'Precision Steel Bearing Balls', 'Precision Steel Bearing Balls', '', ( #5521 ) ) ;
#3914=ORIENTED_EDGE ( 'NONE', *, *, #370, .F. ) ;
#3928=PRESENTATION_STYLE_ASSIGNMENT (( #5871 ) ) ;
#4298=DIRECTION ( 'NONE',  ( 1.000000000000000000, 1.224646799147352961E-16, 0.000000000000000000 ) ) ;
#4567=COLOUR_RGB ( '', 0.40784314, 0.44705882, 0.49803922) ;
#4717=AXIS2_PLACEMENT_3D ( 'NONE', #240, #3557, #4298 ) ;
#4944=ORIENTED_EDGE ( 'NONE', *, *, #9904, .F. ) ;
#4987=DIRECTION ( 'NONE',  ( 0.000000000000000000, -1.000000000000000000, 0.000000000000000000 ) ) ;
#5381=CIRCLE ( 'NONE', #4717, 9.900000000000002132 ) ;
#5521=PRODUCT_CONTEXT ( 'NONE', #12327, 'mechanical' ) ;
#5552=PRODUCT_DEFINITION_FORMATION_WITH_SPECIFIED_SOURCE ( 'ANY', '', #3805, .NOT_KNOWN. ) ;
#5613=DIRECTION ( 'NONE',  ( 1.000000000000000000, 0.000000000000000000, 0.000000000000000000 ) ) ;
#5871=SURFACE_STYLE_USAGE ( .BOTH. , #2781 ) ;
#5911=MANIFOLD_SOLID_BREP ( 'NONE', #7524 ) ;
#5987=UNCERTAINTY_MEASURE_WITH_UNIT (LENGTH_MEASURE( 1.000000000000000082E-05 ), #867, 'distance_accuracy_value', 'NONE');
#6298=FACE_OUTER_BOUND ( 'NONE', #2271, .T. ) ;
#6711=CARTESIAN_POINT ( 'NONE',  ( 0.000000000000000000, 0.000000000000000000, 0.000000000000000000 ) ) ;
#6860=EDGE_LOOP ( 'NONE', ( #4944, #1839 ) ) ;
#7356=CARTESIAN_POINT ( 'NONE',  ( 11.00000000000000000, 0.000000000000000000, 250.0000000000000000 ) ) ;
#7357=UNCERTAINTY_MEASURE_WITH_UNIT (LENGTH_MEASURE( 1.000000000000000082E-05 ), #9033, 'distance_accuracy_value', 'NONE');
#7414=SPHERICAL_SURFACE ( 'NONE', #3116, 9.900000000000000355 ) ;
#7524=CLOSED_SHELL ( 'NONE', ( #346, #12600 ) ) ;
#7873=CARTESIAN_POINT ( 'NONE',  ( 11.00000000000000000, 0.000000000000000000, 250.0000000000000000 ) ) ;
#7929=FILL_AREA_STYLE ('',( #9999 ) ) ;
#8833=( NAMED_UNIT ( * ) PLANE_ANGLE_UNIT ( ) SI_UNIT ( $, .RADIAN. ) );
#9033=( LENGTH_UNIT ( ) NAMED_UNIT ( * ) SI_UNIT ( .MILLI., .METRE. ) );
#9051=( GEOMETRIC_REPRESENTATION_CONTEXT ( 3 ) GLOBAL_UNCERTAINTY_ASSIGNED_CONTEXT ( ( #5987 ) ) GLOBAL_UNIT_ASSIGNED_CONTEXT ( ( #867, #12005, #9066 ) ) REPRESENTATION_CONTEXT ( 'NONE', 'WORKASPACE' ) );
#9066=( NAMED_UNIT ( * ) SI_UNIT ( $, .STERADIAN. ) SOLID_ANGLE_UNIT ( ) );
#9126=SURFACE_STYLE_FILL_AREA ( #7929 ) ;
#9287=ORIENTED_EDGE ( 'NONE', *, *, #9904, .T. ) ;
#9579=SHAPE_DEFINITION_REPRESENTATION ( #1793, #182 ) ;
#9904=EDGE_CURVE ( 'NONE', #690, #1431, #5381, .T. ) ;
#9999=FILL_AREA_STYLE_COLOUR ( '', #4567 ) ;
#10287=( NAMED_UNIT ( * ) SI_UNIT ( $, .STERADIAN. ) SOLID_ANGLE_UNIT ( ) );
#10635=DIRECTION ( 'NONE',  ( 1.000000000000000000, 0.000000000000000000, 0.000000000000000000 ) ) ;
#10765=DIRECTION ( 'NONE',  ( 0.000000000000000000, 0.000000000000000000, 1.000000000000000000 ) ) ;
#10874=DIRECTION ( 'NONE',  ( -0.000000000000000000, 1.000000000000000000, 0.000000000000000000 ) ) ;
#11004=CIRCLE ( 'NONE', #3758, 9.900000000000019895 ) ;
#11059=CARTESIAN_POINT ( 'NONE',  ( 11.00000000000000000, 0.000000000000000000, 250.0000000000000000 ) ) ;
#11070=AXIS2_PLACEMENT_3D ( 'NONE', #11059, #4987, #1930 ) ;
#11264=ADVANCED_BREP_SHAPE_REPRESENTATION ( '', ( #5911, #805 ), #1451 ) ;
#11489=DIRECTION ( 'NONE',  ( 0.000000000000000000, -1.000000000000000000, 0.000000000000000000 ) ) ;
#12002=FACE_OUTER_BOUND ( 'NONE', #6860, .T. ) ;
#12005=( NAMED_UNIT ( * ) PLANE_ANGLE_UNIT ( ) SI_UNIT ( $, .RADIAN. ) );
#12069=PRODUCT_DEFINITION ( 'UNKNOWN', '', #5552, #292 ) ;
#12301=APPLICATION_CONTEXT ( 'automotive_design' ) ;
#12327=APPLICATION_CONTEXT ( 'automotive_design' ) ;
#12459=STYLED_ITEM ( 'NONE', ( #3928 ), #5911 ) ;
#12600=ADVANCED_FACE ( 'NONE', ( #12002 ), #2848, .T. ) ;
#12938=DIRECTION ( 'NONE',  ( 0.000000000000000000, 0.000000000000000000, 1.000000000000000000 ) ) ;
#13015=CARTESIAN_POINT ( 'NONE',  ( 11.00000000000000000, 0.000000000000000000, 240.0999999999999943 ) ) ;
ENDSEC;
END-ISO-10303-21;
